ISO-10303-21;
HEADER;
/* Generated by software containing ST-Developer
 * from STEP Tools, Inc. (www.steptools.com) 
 */

FILE_DESCRIPTION(
/* description */ ('PAT-083'),
/* implementation_level */ '2;1');

FILE_NAME(
/* name */ 'Diaphragm.step',
/* time_stamp */ '2026-10-29T20:18:00-07:00',
/* author */ (''),
/* organization */ (''),
/* preprocessor_version */ 'ST-DEVELOPER v20.2',
/* originating_system */ 'Autodesk Translation Framework v15.17.0.0',
/* authorisation */ '');

FILE_SCHEMA (('AUTOMOTIVE_DESIGN { 1 0 10303 214 3 1 1 }'));
ENDSEC;

DATA;
#10=MECHANICAL_DESIGN_GEOMETRIC_PRESENTATION_REPRESENTATION('',(#238),#8428);
#190=SHAPE_REPRESENTATION_RELATIONSHIP('SRR','None',#8524,#214);
#214=ADVANCED_BREP_SHAPE_REPRESENTATION('',(#262),#8413);
#238=STYLED_ITEM('',(#8719),#262);
#262=MANIFOLD_SOLID_BREP('Body1',#3684);
#306=FACE_BOUND('',#851,.T.);
#307=FACE_BOUND('',#852,.T.);
#308=FACE_BOUND('',#853,.T.);
#309=FACE_BOUND('',#854,.T.);
#310=FACE_BOUND('',#855,.T.);
#311=FACE_BOUND('',#856,.T.);
#312=FACE_BOUND('',#857,.T.);
#313=FACE_BOUND('',#859,.T.);
#314=FACE_BOUND('',#860,.T.);
#315=FACE_BOUND('',#861,.T.);
#316=FACE_BOUND('',#862,.T.);
#317=FACE_BOUND('',#863,.T.);
#318=FACE_BOUND('',#864,.T.);
#319=FACE_BOUND('',#865,.T.);
#405=PLANE('',#4147);
#406=PLANE('',#4148);
#578=FACE_OUTER_BOUND('',#842,.T.);
#579=FACE_OUTER_BOUND('',#843,.T.);
#580=FACE_OUTER_BOUND('',#844,.T.);
#581=FACE_OUTER_BOUND('',#845,.T.);
#582=FACE_OUTER_BOUND('',#846,.T.);
#583=FACE_OUTER_BOUND('',#847,.T.);
#584=FACE_OUTER_BOUND('',#848,.T.);
#585=FACE_OUTER_BOUND('',#849,.T.);
#586=FACE_OUTER_BOUND('',#850,.T.);
#587=FACE_OUTER_BOUND('',#858,.T.);
#842=EDGE_LOOP('',(#2756,#2757,#2758,#2759));
#843=EDGE_LOOP('',(#2760,#2761,#2762,#2763));
#844=EDGE_LOOP('',(#2764,#2765,#2766,#2767));
#845=EDGE_LOOP('',(#2768,#2769,#2770,#2771));
#846=EDGE_LOOP('',(#2772,#2773,#2774,#2775));
#847=EDGE_LOOP('',(#2776,#2777,#2778,#2779));
#848=EDGE_LOOP('',(#2780,#2781,#2782,#2783));
#849=EDGE_LOOP('',(#2784,#2785,#2786,#2787));
#850=EDGE_LOOP('',(#2788));
#851=EDGE_LOOP('',(#2789));
#852=EDGE_LOOP('',(#2790));
#853=EDGE_LOOP('',(#2791));
#854=EDGE_LOOP('',(#2792));
#855=EDGE_LOOP('',(#2793));
#856=EDGE_LOOP('',(#2794));
#857=EDGE_LOOP('',(#2795));
#858=EDGE_LOOP('',(#2796));
#859=EDGE_LOOP('',(#2797));
#860=EDGE_LOOP('',(#2798));
#861=EDGE_LOOP('',(#2799));
#862=EDGE_LOOP('',(#2800));
#863=EDGE_LOOP('',(#2801));
#864=EDGE_LOOP('',(#2802));
#865=EDGE_LOOP('',(#2803));
#1117=LINE('',#6830,#1361);
#1118=LINE('',#6836,#1362);
#1119=LINE('',#6842,#1363);
#1120=LINE('',#6848,#1364);
#1121=LINE('',#6854,#1365);
#1122=LINE('',#6860,#1366);
#1123=LINE('',#6866,#1367);
#1124=LINE('',#6872,#1368);
#1361=VECTOR('',#4829,0.275);
#1362=VECTOR('',#4836,0.275);
#1363=VECTOR('',#4843,0.275);
#1364=VECTOR('',#4850,0.275);
#1365=VECTOR('',#4857,0.275);
#1366=VECTOR('',#4864,0.275);
#1367=VECTOR('',#4871,0.16);
#1368=VECTOR('',#4878,4.);
#1594=CIRCLE('',#4124,0.275);
#1595=CIRCLE('',#4125,0.275);
#1596=CIRCLE('',#4127,0.275);
#1597=CIRCLE('',#4128,0.275);
#1598=CIRCLE('',#4130,0.275);
#1599=CIRCLE('',#4131,0.275);
#1600=CIRCLE('',#4133,0.275);
#1601=CIRCLE('',#4134,0.275);
#1602=CIRCLE('',#4136,0.275);
#1603=CIRCLE('',#4137,0.275);
#1604=CIRCLE('',#4139,0.275);
#1605=CIRCLE('',#4140,0.275);
#1606=CIRCLE('',#4142,0.16);
#1607=CIRCLE('',#4143,0.16);
#1608=CIRCLE('',#4145,4.);
#1609=CIRCLE('',#4146,4.);
#1807=VERTEX_POINT('',#6827);
#1808=VERTEX_POINT('',#6829);
#1809=VERTEX_POINT('',#6833);
#1810=VERTEX_POINT('',#6835);
#1811=VERTEX_POINT('',#6839);
#1812=VERTEX_POINT('',#6841);
#1813=VERTEX_POINT('',#6845);
#1814=VERTEX_POINT('',#6847);
#1815=VERTEX_POINT('',#6851);
#1816=VERTEX_POINT('',#6853);
#1817=VERTEX_POINT('',#6857);
#1818=VERTEX_POINT('',#6859);
#1819=VERTEX_POINT('',#6863);
#1820=VERTEX_POINT('',#6865);
#1821=VERTEX_POINT('',#6869);
#1822=VERTEX_POINT('',#6871);
#2154=EDGE_CURVE('',#1807,#1807,#1594,.T.);
#2155=EDGE_CURVE('',#1807,#1808,#1117,.T.);
#2156=EDGE_CURVE('',#1808,#1808,#1595,.T.);
#2157=EDGE_CURVE('',#1809,#1809,#1596,.T.);
#2158=EDGE_CURVE('',#1809,#1810,#1118,.T.);
#2159=EDGE_CURVE('',#1810,#1810,#1597,.T.);
#2160=EDGE_CURVE('',#1811,#1811,#1598,.T.);
#2161=EDGE_CURVE('',#1811,#1812,#1119,.T.);
#2162=EDGE_CURVE('',#1812,#1812,#1599,.T.);
#2163=EDGE_CURVE('',#1813,#1813,#1600,.T.);
#2164=EDGE_CURVE('',#1813,#1814,#1120,.T.);
#2165=EDGE_CURVE('',#1814,#1814,#1601,.T.);
#2166=EDGE_CURVE('',#1815,#1815,#1602,.T.);
#2167=EDGE_CURVE('',#1815,#1816,#1121,.T.);
#2168=EDGE_CURVE('',#1816,#1816,#1603,.T.);
#2169=EDGE_CURVE('',#1817,#1817,#1604,.T.);
#2170=EDGE_CURVE('',#1817,#1818,#1122,.T.);
#2171=EDGE_CURVE('',#1818,#1818,#1605,.T.);
#2172=EDGE_CURVE('',#1819,#1819,#1606,.T.);
#2173=EDGE_CURVE('',#1819,#1820,#1123,.T.);
#2174=EDGE_CURVE('',#1820,#1820,#1607,.T.);
#2175=EDGE_CURVE('',#1821,#1821,#1608,.T.);
#2176=EDGE_CURVE('',#1821,#1822,#1124,.T.);
#2177=EDGE_CURVE('',#1822,#1822,#1609,.T.);
#2756=ORIENTED_EDGE('',*,*,#2154,.F.);
#2757=ORIENTED_EDGE('',*,*,#2155,.T.);
#2758=ORIENTED_EDGE('',*,*,#2156,.F.);
#2759=ORIENTED_EDGE('',*,*,#2155,.F.);
#2760=ORIENTED_EDGE('',*,*,#2157,.F.);
#2761=ORIENTED_EDGE('',*,*,#2158,.T.);
#2762=ORIENTED_EDGE('',*,*,#2159,.F.);
#2763=ORIENTED_EDGE('',*,*,#2158,.F.);
#2764=ORIENTED_EDGE('',*,*,#2160,.F.);
#2765=ORIENTED_EDGE('',*,*,#2161,.T.);
#2766=ORIENTED_EDGE('',*,*,#2162,.F.);
#2767=ORIENTED_EDGE('',*,*,#2161,.F.);
#2768=ORIENTED_EDGE('',*,*,#2163,.F.);
#2769=ORIENTED_EDGE('',*,*,#2164,.T.);
#2770=ORIENTED_EDGE('',*,*,#2165,.F.);
#2771=ORIENTED_EDGE('',*,*,#2164,.F.);
#2772=ORIENTED_EDGE('',*,*,#2166,.F.);
#2773=ORIENTED_EDGE('',*,*,#2167,.T.);
#2774=ORIENTED_EDGE('',*,*,#2168,.F.);
#2775=ORIENTED_EDGE('',*,*,#2167,.F.);
#2776=ORIENTED_EDGE('',*,*,#2169,.F.);
#2777=ORIENTED_EDGE('',*,*,#2170,.T.);
#2778=ORIENTED_EDGE('',*,*,#2171,.F.);
#2779=ORIENTED_EDGE('',*,*,#2170,.F.);
#2780=ORIENTED_EDGE('',*,*,#2172,.F.);
#2781=ORIENTED_EDGE('',*,*,#2173,.T.);
#2782=ORIENTED_EDGE('',*,*,#2174,.T.);
#2783=ORIENTED_EDGE('',*,*,#2173,.F.);
#2784=ORIENTED_EDGE('',*,*,#2175,.F.);
#2785=ORIENTED_EDGE('',*,*,#2176,.T.);
#2786=ORIENTED_EDGE('',*,*,#2177,.T.);
#2787=ORIENTED_EDGE('',*,*,#2176,.F.);
#2788=ORIENTED_EDGE('',*,*,#2175,.T.);
#2789=ORIENTED_EDGE('',*,*,#2172,.T.);
#2790=ORIENTED_EDGE('',*,*,#2171,.T.);
#2791=ORIENTED_EDGE('',*,*,#2168,.T.);
#2792=ORIENTED_EDGE('',*,*,#2165,.T.);
#2793=ORIENTED_EDGE('',*,*,#2162,.T.);
#2794=ORIENTED_EDGE('',*,*,#2159,.T.);
#2795=ORIENTED_EDGE('',*,*,#2156,.T.);
#2796=ORIENTED_EDGE('',*,*,#2177,.F.);
#2797=ORIENTED_EDGE('',*,*,#2174,.F.);
#2798=ORIENTED_EDGE('',*,*,#2169,.T.);
#2799=ORIENTED_EDGE('',*,*,#2166,.T.);
#2800=ORIENTED_EDGE('',*,*,#2163,.T.);
#2801=ORIENTED_EDGE('',*,*,#2160,.T.);
#2802=ORIENTED_EDGE('',*,*,#2157,.T.);
#2803=ORIENTED_EDGE('',*,*,#2154,.T.);
#3397=CYLINDRICAL_SURFACE('',#4123,0.275);
#3398=CYLINDRICAL_SURFACE('',#4126,0.275);
#3399=CYLINDRICAL_SURFACE('',#4129,0.275);
#3400=CYLINDRICAL_SURFACE('',#4132,0.275);
#3401=CYLINDRICAL_SURFACE('',#4135,0.275);
#3402=CYLINDRICAL_SURFACE('',#4138,0.275);
#3403=CYLINDRICAL_SURFACE('',#4141,0.16);
#3404=CYLINDRICAL_SURFACE('',#4144,4.);
#3525=ADVANCED_FACE('',(#578),#3397,.F.);
#3526=ADVANCED_FACE('',(#579),#3398,.F.);
#3527=ADVANCED_FACE('',(#580),#3399,.F.);
#3528=ADVANCED_FACE('',(#581),#3400,.F.);
#3529=ADVANCED_FACE('',(#582),#3401,.F.);
#3530=ADVANCED_FACE('',(#583),#3402,.F.);
#3531=ADVANCED_FACE('',(#584),#3403,.F.);
#3532=ADVANCED_FACE('',(#585),#3404,.T.);
#3533=ADVANCED_FACE('',(#586,#306,#307,#308,#309,#310,#311,#312),#405,.T.);
#3534=ADVANCED_FACE('',(#587,#313,#314,#315,#316,#317,#318,#319),#406,.F.);
#3684=CLOSED_SHELL('',(#3525,#3526,#3527,#3528,#3529,#3530,#3531,#3532,
#3533,#3534));
#4122=AXIS2_PLACEMENT_3D('',#6825,#4823,#4824);
#4123=AXIS2_PLACEMENT_3D('',#6826,#4825,#4826);
#4124=AXIS2_PLACEMENT_3D('',#6828,#4827,#4828);
#4125=AXIS2_PLACEMENT_3D('',#6831,#4830,#4831);
#4126=AXIS2_PLACEMENT_3D('',#6832,#4832,#4833);
#4127=AXIS2_PLACEMENT_3D('',#6834,#4834,#4835);
#4128=AXIS2_PLACEMENT_3D('',#6837,#4837,#4838);
#4129=AXIS2_PLACEMENT_3D('',#6838,#4839,#4840);
#4130=AXIS2_PLACEMENT_3D('',#6840,#4841,#4842);
#4131=AXIS2_PLACEMENT_3D('',#6843,#4844,#4845);
#4132=AXIS2_PLACEMENT_3D('',#6844,#4846,#4847);
#4133=AXIS2_PLACEMENT_3D('',#6846,#4848,#4849);
#4134=AXIS2_PLACEMENT_3D('',#6849,#4851,#4852);
#4135=AXIS2_PLACEMENT_3D('',#6850,#4853,#4854);
#4136=AXIS2_PLACEMENT_3D('',#6852,#4855,#4856);
#4137=AXIS2_PLACEMENT_3D('',#6855,#4858,#4859);
#4138=AXIS2_PLACEMENT_3D('',#6856,#4860,#4861);
#4139=AXIS2_PLACEMENT_3D('',#6858,#4862,#4863);
#4140=AXIS2_PLACEMENT_3D('',#6861,#4865,#4866);
#4141=AXIS2_PLACEMENT_3D('',#6862,#4867,#4868);
#4142=AXIS2_PLACEMENT_3D('',#6864,#4869,#4870);
#4143=AXIS2_PLACEMENT_3D('',#6867,#4872,#4873);
#4144=AXIS2_PLACEMENT_3D('',#6868,#4874,#4875);
#4145=AXIS2_PLACEMENT_3D('',#6870,#4876,#4877);
#4146=AXIS2_PLACEMENT_3D('',#6873,#4879,#4880);
#4147=AXIS2_PLACEMENT_3D('',#6874,#4881,#4882);
#4148=AXIS2_PLACEMENT_3D('',#6875,#4883,#4884);
#4823=DIRECTION('axis',(0.,0.,1.));
#4824=DIRECTION('refdir',(1.,0.,0.));
#4825=DIRECTION('center_axis',(0.,0.,1.));
#4826=DIRECTION('ref_axis',(1.,0.,0.));
#4827=DIRECTION('center_axis',(0.,0.,1.));
#4828=DIRECTION('ref_axis',(1.,0.,0.));
#4829=DIRECTION('',(0.,0.,1.));
#4830=DIRECTION('center_axis',(0.,0.,-1.));
#4831=DIRECTION('ref_axis',(1.,0.,0.));
#4832=DIRECTION('center_axis',(0.,0.,1.));
#4833=DIRECTION('ref_axis',(1.,0.,0.));
#4834=DIRECTION('center_axis',(0.,0.,1.));
#4835=DIRECTION('ref_axis',(1.,0.,0.));
#4836=DIRECTION('',(0.,0.,1.));
#4837=DIRECTION('center_axis',(0.,0.,-1.));
#4838=DIRECTION('ref_axis',(1.,0.,0.));
#4839=DIRECTION('center_axis',(0.,0.,1.));
#4840=DIRECTION('ref_axis',(1.,0.,0.));
#4841=DIRECTION('center_axis',(0.,0.,1.));
#4842=DIRECTION('ref_axis',(1.,0.,0.));
#4843=DIRECTION('',(0.,0.,1.));
#4844=DIRECTION('center_axis',(0.,0.,-1.));
#4845=DIRECTION('ref_axis',(1.,0.,0.));
#4846=DIRECTION('center_axis',(0.,0.,1.));
#4847=DIRECTION('ref_axis',(1.,0.,0.));
#4848=DIRECTION('center_axis',(0.,0.,1.));
#4849=DIRECTION('ref_axis',(1.,0.,0.));
#4850=DIRECTION('',(0.,0.,1.));
#4851=DIRECTION('center_axis',(0.,0.,-1.));
#4852=DIRECTION('ref_axis',(1.,0.,0.));
#4853=DIRECTION('center_axis',(0.,0.,1.));
#4854=DIRECTION('ref_axis',(1.,0.,0.));
#4855=DIRECTION('center_axis',(0.,0.,1.));
#4856=DIRECTION('ref_axis',(1.,0.,0.));
#4857=DIRECTION('',(0.,0.,1.));
#4858=DIRECTION('center_axis',(0.,0.,-1.));
#4859=DIRECTION('ref_axis',(1.,0.,0.));
#4860=DIRECTION('center_axis',(0.,0.,1.));
#4861=DIRECTION('ref_axis',(1.,0.,0.));
#4862=DIRECTION('center_axis',(0.,0.,1.));
#4863=DIRECTION('ref_axis',(1.,0.,0.));
#4864=DIRECTION('',(0.,0.,1.));
#4865=DIRECTION('center_axis',(0.,0.,-1.));
#4866=DIRECTION('ref_axis',(1.,0.,0.));
#4867=DIRECTION('center_axis',(0.,0.,1.));
#4868=DIRECTION('ref_axis',(1.,0.,0.));
#4869=DIRECTION('center_axis',(0.,0.,-1.));
#4870=DIRECTION('ref_axis',(1.,0.,0.));
#4871=DIRECTION('',(0.,0.,-1.));
#4872=DIRECTION('center_axis',(0.,0.,-1.));
#4873=DIRECTION('ref_axis',(1.,0.,0.));
#4874=DIRECTION('center_axis',(0.,0.,1.));
#4875=DIRECTION('ref_axis',(1.,0.,0.));
#4876=DIRECTION('center_axis',(0.,0.,1.));
#4877=DIRECTION('ref_axis',(1.,0.,0.));
#4878=DIRECTION('',(0.,0.,-1.));
#4879=DIRECTION('center_axis',(0.,0.,1.));
#4880=DIRECTION('ref_axis',(1.,0.,0.));
#4881=DIRECTION('center_axis',(0.,0.,1.));
#4882=DIRECTION('ref_axis',(1.,0.,0.));
#4883=DIRECTION('center_axis',(0.,0.,1.));
#4884=DIRECTION('ref_axis',(1.,0.,0.));
#6825=CARTESIAN_POINT('',(0.,0.,0.));
#6826=CARTESIAN_POINT('Origin',(-6.2456986756515E-16,-3.4,4.9));
#6827=CARTESIAN_POINT('',(-0.275000000000001,-3.4,5.));
#6828=CARTESIAN_POINT('Origin',(-6.2456986756515E-16,-3.4,5.));
#6829=CARTESIAN_POINT('',(-0.275000000000001,-3.4,5.1));
#6830=CARTESIAN_POINT('',(-0.275000000000001,-3.4,4.9));
#6831=CARTESIAN_POINT('Origin',(-6.2456986756515E-16,-3.4,5.1));
#6832=CARTESIAN_POINT('Origin',(2.94448637286709,1.7,4.9));
#6833=CARTESIAN_POINT('',(2.66948637286709,1.7,5.));
#6834=CARTESIAN_POINT('Origin',(2.94448637286709,1.7,5.));
#6835=CARTESIAN_POINT('',(2.66948637286709,1.7,5.1));
#6836=CARTESIAN_POINT('',(2.66948637286709,1.7,4.9));
#6837=CARTESIAN_POINT('Origin',(2.94448637286709,1.7,5.1));
#6838=CARTESIAN_POINT('Origin',(2.0818995585505E-16,3.4,4.9));
#6839=CARTESIAN_POINT('',(-0.275,3.4,5.));
#6840=CARTESIAN_POINT('Origin',(2.0818995585505E-16,3.4,5.));
#6841=CARTESIAN_POINT('',(-0.275,3.4,5.1));
#6842=CARTESIAN_POINT('',(-0.275,3.4,4.9));
#6843=CARTESIAN_POINT('Origin',(2.0818995585505E-16,3.4,5.1));
#6844=CARTESIAN_POINT('Origin',(-2.94448637286709,1.7,4.9));
#6845=CARTESIAN_POINT('',(-3.21948637286709,1.7,5.));
#6846=CARTESIAN_POINT('Origin',(-2.94448637286709,1.7,5.));
#6847=CARTESIAN_POINT('',(-3.21948637286709,1.7,5.1));
#6848=CARTESIAN_POINT('',(-3.21948637286709,1.7,4.9));
#6849=CARTESIAN_POINT('Origin',(-2.94448637286709,1.7,5.1));
#6850=CARTESIAN_POINT('Origin',(-2.94448637286709,-1.7,4.9));
#6851=CARTESIAN_POINT('',(-3.21948637286709,-1.7,5.));
#6852=CARTESIAN_POINT('Origin',(-2.94448637286709,-1.7,5.));
#6853=CARTESIAN_POINT('',(-3.21948637286709,-1.7,5.1));
#6854=CARTESIAN_POINT('',(-3.21948637286709,-1.7,4.9));
#6855=CARTESIAN_POINT('Origin',(-2.94448637286709,-1.7,5.1));
#6856=CARTESIAN_POINT('Origin',(2.94448637286709,-1.7,4.9));
#6857=CARTESIAN_POINT('',(2.66948637286709,-1.7,5.));
#6858=CARTESIAN_POINT('Origin',(2.94448637286709,-1.7,5.));
#6859=CARTESIAN_POINT('',(2.66948637286709,-1.7,5.1));
#6860=CARTESIAN_POINT('',(2.66948637286709,-1.7,4.9));
#6861=CARTESIAN_POINT('Origin',(2.94448637286709,-1.7,5.1));
#6862=CARTESIAN_POINT('Origin',(0.,0.,5.));
#6863=CARTESIAN_POINT('',(-0.16,-1.95943487863577E-17,5.1));
#6864=CARTESIAN_POINT('Origin',(0.,0.,5.1));
#6865=CARTESIAN_POINT('',(-0.16,-1.95943487863577E-17,5.));
#6866=CARTESIAN_POINT('',(-0.16,-1.95943487863577E-17,5.));
#6867=CARTESIAN_POINT('Origin',(0.,0.,5.));
#6868=CARTESIAN_POINT('Origin',(0.,0.,5.));
#6869=CARTESIAN_POINT('',(-4.,-4.89858719658941E-16,5.1));
#6870=CARTESIAN_POINT('Origin',(0.,0.,5.1));
#6871=CARTESIAN_POINT('',(-4.,-4.89858719658941E-16,5.));
#6872=CARTESIAN_POINT('',(-4.,-4.89858719658941E-16,5.));
#6873=CARTESIAN_POINT('Origin',(0.,0.,5.));
#6874=CARTESIAN_POINT('Origin',(0.,0.,5.1));
#6875=CARTESIAN_POINT('Origin',(0.,0.,5.));
#8387=UNCERTAINTY_MEASURE_WITH_UNIT(LENGTH_MEASURE(0.001),#8429,
'DISTANCE_ACCURACY_VALUE',
'Maximum model space distance between geometric entities at asserted c
onnectivities');
#8402=UNCERTAINTY_MEASURE_WITH_UNIT(LENGTH_MEASURE(0.001),#8429,
'DISTANCE_ACCURACY_VALUE',
'Maximum model space distance between geometric entities at asserted c
onnectivities');
#8413=(
GEOMETRIC_REPRESENTATION_CONTEXT(3)
GLOBAL_UNCERTAINTY_ASSIGNED_CONTEXT((#8387))
GLOBAL_UNIT_ASSIGNED_CONTEXT((#8429,#8431,#8432))
REPRESENTATION_CONTEXT('','3D')
);
#8428=(
GEOMETRIC_REPRESENTATION_CONTEXT(3)
GLOBAL_UNCERTAINTY_ASSIGNED_CONTEXT((#8402))
GLOBAL_UNIT_ASSIGNED_CONTEXT((#8429,#8431,#8432))
REPRESENTATION_CONTEXT('','3D')
);
#8429=(
LENGTH_UNIT()
NAMED_UNIT(*)
SI_UNIT(.CENTI.,.METRE.)
);
#8431=(
NAMED_UNIT(*)
PLANE_ANGLE_UNIT()
SI_UNIT($,.RADIAN.)
);
#8432=(
NAMED_UNIT(*)
SI_UNIT($,.STERADIAN.)
SOLID_ANGLE_UNIT()
);
#8443=SHAPE_DEFINITION_REPRESENTATION(#8468,#8524);
#8468=PRODUCT_DEFINITION_SHAPE('',$,#8550);
#8524=SHAPE_REPRESENTATION('',(#4122),#8413);
#8539=PRODUCT_DEFINITION_CONTEXT('part definition',#8616,'design');
#8550=PRODUCT_DEFINITION('Diaphragm','Diaphragm',#8575,
#8539);
#8575=PRODUCT_DEFINITION_FORMATION('',$,#8628);
#8616=APPLICATION_CONTEXT(
'Core Data for Automotive Mechanical Design Process');
#8617=PRODUCT_CONTEXT('part definition',#8616,'mechanical');
#8628=PRODUCT('Diaphragm','Diaphragm','Diaphragm',(#8617));
#8713=COLOUR_RGB('Off White',0.89,0.88,0.83);
#8714=FILL_AREA_STYLE_COLOUR('',#8713);
#8715=FILL_AREA_STYLE('',(#8714));
#8716=SURFACE_STYLE_FILL_AREA(#8715);
#8717=SURFACE_SIDE_STYLE('',(#8716));
#8718=SURFACE_STYLE_USAGE(.BOTH.,#8717);
#8719=PRESENTATION_STYLE_ASSIGNMENT((#8718));
ENDSEC;
END-ISO-10303-21;
